ISO-10303-21;
HEADER;
/* Generated by software containing ST-Developer
 * from STEP Tools, Inc. (www.steptools.com) 
 */

FILE_DESCRIPTION(
/* description */ ('PAT-026'),
/* implementation_level */ '2;1');

FILE_NAME(
/* name */ 'Cap Screw - M4x16.step',
/* time_stamp */ '2026-10-28T22:25:58-07:00',
/* author */ (''),
/* organization */ (''),
/* preprocessor_version */ 'ST-DEVELOPER v20.2',
/* originating_system */ 'Autodesk Translation Framework v15.17.0.0',
/* authorisation */ '');

FILE_SCHEMA (('AUTOMOTIVE_DESIGN { 1 0 10303 214 3 1 1 }'));
ENDSEC;

DATA;
#10=MECHANICAL_DESIGN_GEOMETRIC_PRESENTATION_REPRESENTATION('',(#146),#12343);
#107=CONICAL_SURFACE('',#7579,0.325,0.785398163397448);
#108=CONICAL_SURFACE('',#7583,0.335,0.785398163397448);
#109=CONICAL_SURFACE('',#7587,0.21,0.463647609000806);
#110=CONICAL_SURFACE('',#7591,0.18,0.785398163397448);
#116=ORIENTED_CLOSED_SHELL('',*,#7354,.F.);
#118=BREP_WITH_VOIDS('Body1',#7353,(#116));
#124=SHAPE_REPRESENTATION_RELATIONSHIP('SRR','None',#12401,#135);
#135=ADVANCED_BREP_SHAPE_REPRESENTATION('',(#118),#12336);
#146=STYLED_ITEM('',(#12540),#118);
#180=FACE_BOUND('',#1035,.T.);
#231=PLANE('',#7577);
#232=PLANE('',#7585);
#233=PLANE('',#7593);
#234=PLANE('',#7594);
#235=PLANE('',#7595);
#236=PLANE('',#7596);
#237=PLANE('',#7597);
#238=PLANE('',#7598);
#239=PLANE('',#7599);
#240=PLANE('',#7600);
#241=PLANE('',#7601);
#608=FACE_OUTER_BOUND('',#1030,.T.);
#609=FACE_OUTER_BOUND('',#1031,.T.);
#610=FACE_OUTER_BOUND('',#1032,.T.);
#611=FACE_OUTER_BOUND('',#1033,.T.);
#612=FACE_OUTER_BOUND('',#1034,.T.);
#613=FACE_OUTER_BOUND('',#1036,.T.);
#614=FACE_OUTER_BOUND('',#1037,.T.);
#615=FACE_OUTER_BOUND('',#1038,.T.);
#616=FACE_OUTER_BOUND('',#1039,.T.);
#617=FACE_OUTER_BOUND('',#1040,.T.);
#618=FACE_OUTER_BOUND('',#1041,.T.);
#619=FACE_OUTER_BOUND('',#1042,.T.);
#620=FACE_OUTER_BOUND('',#1043,.T.);
#621=FACE_OUTER_BOUND('',#1044,.T.);
#622=FACE_OUTER_BOUND('',#1045,.T.);
#623=FACE_OUTER_BOUND('',#1046,.T.);
#624=FACE_OUTER_BOUND('',#1047,.T.);
#1030=EDGE_LOOP('',(#5145));
#1031=EDGE_LOOP('',(#5146,#5147,#5148,#5149));
#1032=EDGE_LOOP('',(#5150,#5151,#5152,#5153));
#1033=EDGE_LOOP('',(#5154,#5155,#5156,#5157));
#1034=EDGE_LOOP('',(#5158));
#1035=EDGE_LOOP('',(#5159));
#1036=EDGE_LOOP('',(#5160,#5161,#5162,#5163));
#1037=EDGE_LOOP('',(#5164,#5165,#5166,#5167));
#1038=EDGE_LOOP('',(#5168,#5169,#5170,#5171));
#1039=EDGE_LOOP('',(#5172));
#1040=EDGE_LOOP('',(#5173,#5174,#5175,#5176));
#1041=EDGE_LOOP('',(#5177,#5178,#5179,#5180));
#1042=EDGE_LOOP('',(#5181,#5182,#5183,#5184));
#1043=EDGE_LOOP('',(#5185,#5186,#5187,#5188));
#1044=EDGE_LOOP('',(#5189,#5190,#5191,#5192));
#1045=EDGE_LOOP('',(#5193,#5194,#5195,#5196));
#1046=EDGE_LOOP('',(#5197,#5198,#5199,#5200,#5201,#5202));
#1047=EDGE_LOOP('',(#5203,#5204,#5205,#5206,#5207,#5208));
#1482=LINE('',#10312,#2354);
#1483=LINE('',#10316,#2355);
#1484=LINE('',#10320,#2356);
#1485=LINE('',#10327,#2357);
#1486=LINE('',#10331,#2358);
#1487=LINE('',#10335,#2359);
#1488=LINE('',#10340,#2360);
#1489=LINE('',#10342,#2361);
#1490=LINE('',#10344,#2362);
#1491=LINE('',#10345,#2363);
#1492=LINE('',#10348,#2364);
#1493=LINE('',#10350,#2365);
#1494=LINE('',#10351,#2366);
#1495=LINE('',#10354,#2367);
#1496=LINE('',#10356,#2368);
#1497=LINE('',#10357,#2369);
#1498=LINE('',#10360,#2370);
#1499=LINE('',#10362,#2371);
#1500=LINE('',#10363,#2372);
#1501=LINE('',#10366,#2373);
#1502=LINE('',#10368,#2374);
#1503=LINE('',#10369,#2375);
#1504=LINE('',#10371,#2376);
#1505=LINE('',#10372,#2377);
#2354=VECTOR('',#8332,0.325);
#2355=VECTOR('',#8337,0.35);
#2356=VECTOR('',#8342,0.335);
#2357=VECTOR('',#8351,0.21);
#2358=VECTOR('',#8356,0.2);
#2359=VECTOR('',#8361,0.18);
#2360=VECTOR('',#8366,1.);
#2361=VECTOR('',#8367,1.);
#2362=VECTOR('',#8368,1.);
#2363=VECTOR('',#8369,1.);
#2364=VECTOR('',#8372,1.);
#2365=VECTOR('',#8373,1.);
#2366=VECTOR('',#8374,1.);
#2367=VECTOR('',#8377,1.);
#2368=VECTOR('',#8378,1.);
#2369=VECTOR('',#8379,1.);
#2370=VECTOR('',#8382,1.);
#2371=VECTOR('',#8383,1.);
#2372=VECTOR('',#8384,1.);
#2373=VECTOR('',#8387,1.);
#2374=VECTOR('',#8388,1.);
#2375=VECTOR('',#8389,1.);
#2376=VECTOR('',#8392,1.);
#2377=VECTOR('',#8393,1.);
#3169=CIRCLE('',#7578,0.3);
#3170=CIRCLE('',#7580,0.35);
#3171=CIRCLE('',#7582,0.35);
#3172=CIRCLE('',#7584,0.32);
#3173=CIRCLE('',#7586,0.22);
#3174=CIRCLE('',#7588,0.1954);
#3175=CIRCLE('',#7590,0.1954);
#3176=CIRCLE('',#7592,0.16);
#3342=VERTEX_POINT('',#10307);
#3343=VERTEX_POINT('',#10310);
#3344=VERTEX_POINT('',#10314);
#3345=VERTEX_POINT('',#10318);
#3346=VERTEX_POINT('',#10322);
#3347=VERTEX_POINT('',#10325);
#3348=VERTEX_POINT('',#10329);
#3349=VERTEX_POINT('',#10333);
#3350=VERTEX_POINT('',#10338);
#3351=VERTEX_POINT('',#10339);
#3352=VERTEX_POINT('',#10341);
#3353=VERTEX_POINT('',#10343);
#3354=VERTEX_POINT('',#10347);
#3355=VERTEX_POINT('',#10349);
#3356=VERTEX_POINT('',#10353);
#3357=VERTEX_POINT('',#10355);
#3358=VERTEX_POINT('',#10359);
#3359=VERTEX_POINT('',#10361);
#3360=VERTEX_POINT('',#10365);
#3361=VERTEX_POINT('',#10367);
#4016=EDGE_CURVE('',#3342,#3342,#3169,.T.);
#4017=EDGE_CURVE('',#3343,#3343,#3170,.T.);
#4018=EDGE_CURVE('',#3343,#3342,#1482,.T.);
#4019=EDGE_CURVE('',#3344,#3344,#3171,.T.);
#4020=EDGE_CURVE('',#3344,#3343,#1483,.T.);
#4021=EDGE_CURVE('',#3345,#3345,#3172,.T.);
#4022=EDGE_CURVE('',#3345,#3344,#1484,.T.);
#4023=EDGE_CURVE('',#3346,#3346,#3173,.T.);
#4024=EDGE_CURVE('',#3347,#3347,#3174,.F.);
#4025=EDGE_CURVE('',#3347,#3346,#1485,.T.);
#4026=EDGE_CURVE('',#3348,#3348,#3175,.F.);
#4027=EDGE_CURVE('',#3348,#3347,#1486,.T.);
#4028=EDGE_CURVE('',#3349,#3349,#3176,.T.);
#4029=EDGE_CURVE('',#3349,#3348,#1487,.T.);
#4030=EDGE_CURVE('',#3350,#3351,#1488,.T.);
#4031=EDGE_CURVE('',#3351,#3352,#1489,.T.);
#4032=EDGE_CURVE('',#3352,#3353,#1490,.T.);
#4033=EDGE_CURVE('',#3350,#3353,#1491,.T.);
#4034=EDGE_CURVE('',#3351,#3354,#1492,.T.);
#4035=EDGE_CURVE('',#3354,#3355,#1493,.T.);
#4036=EDGE_CURVE('',#3355,#3352,#1494,.T.);
#4037=EDGE_CURVE('',#3354,#3356,#1495,.T.);
#4038=EDGE_CURVE('',#3356,#3357,#1496,.T.);
#4039=EDGE_CURVE('',#3357,#3355,#1497,.T.);
#4040=EDGE_CURVE('',#3356,#3358,#1498,.T.);
#4041=EDGE_CURVE('',#3358,#3359,#1499,.T.);
#4042=EDGE_CURVE('',#3359,#3357,#1500,.T.);
#4043=EDGE_CURVE('',#3358,#3360,#1501,.T.);
#4044=EDGE_CURVE('',#3360,#3361,#1502,.T.);
#4045=EDGE_CURVE('',#3361,#3359,#1503,.T.);
#4046=EDGE_CURVE('',#3360,#3350,#1504,.T.);
#4047=EDGE_CURVE('',#3353,#3361,#1505,.T.);
#5145=ORIENTED_EDGE('',*,*,#4016,.F.);
#5146=ORIENTED_EDGE('',*,*,#4017,.F.);
#5147=ORIENTED_EDGE('',*,*,#4018,.T.);
#5148=ORIENTED_EDGE('',*,*,#4016,.T.);
#5149=ORIENTED_EDGE('',*,*,#4018,.F.);
#5150=ORIENTED_EDGE('',*,*,#4019,.F.);
#5151=ORIENTED_EDGE('',*,*,#4020,.T.);
#5152=ORIENTED_EDGE('',*,*,#4017,.T.);
#5153=ORIENTED_EDGE('',*,*,#4020,.F.);
#5154=ORIENTED_EDGE('',*,*,#4021,.F.);
#5155=ORIENTED_EDGE('',*,*,#4022,.T.);
#5156=ORIENTED_EDGE('',*,*,#4019,.T.);
#5157=ORIENTED_EDGE('',*,*,#4022,.F.);
#5158=ORIENTED_EDGE('',*,*,#4021,.T.);
#5159=ORIENTED_EDGE('',*,*,#4023,.F.);
#5160=ORIENTED_EDGE('',*,*,#4024,.F.);
#5161=ORIENTED_EDGE('',*,*,#4025,.T.);
#5162=ORIENTED_EDGE('',*,*,#4023,.T.);
#5163=ORIENTED_EDGE('',*,*,#4025,.F.);
#5164=ORIENTED_EDGE('',*,*,#4026,.F.);
#5165=ORIENTED_EDGE('',*,*,#4027,.T.);
#5166=ORIENTED_EDGE('',*,*,#4024,.T.);
#5167=ORIENTED_EDGE('',*,*,#4027,.F.);
#5168=ORIENTED_EDGE('',*,*,#4028,.F.);
#5169=ORIENTED_EDGE('',*,*,#4029,.T.);
#5170=ORIENTED_EDGE('',*,*,#4026,.T.);
#5171=ORIENTED_EDGE('',*,*,#4029,.F.);
#5172=ORIENTED_EDGE('',*,*,#4028,.T.);
#5173=ORIENTED_EDGE('',*,*,#4030,.T.);
#5174=ORIENTED_EDGE('',*,*,#4031,.T.);
#5175=ORIENTED_EDGE('',*,*,#4032,.T.);
#5176=ORIENTED_EDGE('',*,*,#4033,.F.);
#5177=ORIENTED_EDGE('',*,*,#4034,.T.);
#5178=ORIENTED_EDGE('',*,*,#4035,.T.);
#5179=ORIENTED_EDGE('',*,*,#4036,.T.);
#5180=ORIENTED_EDGE('',*,*,#4031,.F.);
#5181=ORIENTED_EDGE('',*,*,#4037,.T.);
#5182=ORIENTED_EDGE('',*,*,#4038,.T.);
#5183=ORIENTED_EDGE('',*,*,#4039,.T.);
#5184=ORIENTED_EDGE('',*,*,#4035,.F.);
#5185=ORIENTED_EDGE('',*,*,#4040,.T.);
#5186=ORIENTED_EDGE('',*,*,#4041,.T.);
#5187=ORIENTED_EDGE('',*,*,#4042,.T.);
#5188=ORIENTED_EDGE('',*,*,#4038,.F.);
#5189=ORIENTED_EDGE('',*,*,#4043,.T.);
#5190=ORIENTED_EDGE('',*,*,#4044,.T.);
#5191=ORIENTED_EDGE('',*,*,#4045,.T.);
#5192=ORIENTED_EDGE('',*,*,#4041,.F.);
#5193=ORIENTED_EDGE('',*,*,#4046,.T.);
#5194=ORIENTED_EDGE('',*,*,#4033,.T.);
#5195=ORIENTED_EDGE('',*,*,#4047,.T.);
#5196=ORIENTED_EDGE('',*,*,#4044,.F.);
#5197=ORIENTED_EDGE('',*,*,#4046,.F.);
#5198=ORIENTED_EDGE('',*,*,#4043,.F.);
#5199=ORIENTED_EDGE('',*,*,#4040,.F.);
#5200=ORIENTED_EDGE('',*,*,#4037,.F.);
#5201=ORIENTED_EDGE('',*,*,#4034,.F.);
#5202=ORIENTED_EDGE('',*,*,#4030,.F.);
#5203=ORIENTED_EDGE('',*,*,#4047,.F.);
#5204=ORIENTED_EDGE('',*,*,#4032,.F.);
#5205=ORIENTED_EDGE('',*,*,#4036,.F.);
#5206=ORIENTED_EDGE('',*,*,#4039,.F.);
#5207=ORIENTED_EDGE('',*,*,#4042,.F.);
#5208=ORIENTED_EDGE('',*,*,#4045,.F.);
#6926=CYLINDRICAL_SURFACE('',#7581,0.35);
#6927=CYLINDRICAL_SURFACE('',#7589,0.1954);
#6999=ADVANCED_FACE('',(#608),#231,.T.);
#7000=ADVANCED_FACE('',(#609),#107,.T.);
#7001=ADVANCED_FACE('',(#610),#6926,.T.);
#7002=ADVANCED_FACE('',(#611),#108,.T.);
#7003=ADVANCED_FACE('',(#612,#180),#232,.T.);
#7004=ADVANCED_FACE('',(#613),#109,.T.);
#7005=ADVANCED_FACE('',(#614),#6927,.T.);
#7006=ADVANCED_FACE('',(#615),#110,.T.);
#7007=ADVANCED_FACE('',(#616),#233,.T.);
#7008=ADVANCED_FACE('',(#617),#234,.F.);
#7009=ADVANCED_FACE('',(#618),#235,.F.);
#7010=ADVANCED_FACE('',(#619),#236,.F.);
#7011=ADVANCED_FACE('',(#620),#237,.F.);
#7012=ADVANCED_FACE('',(#621),#238,.F.);
#7013=ADVANCED_FACE('',(#622),#239,.F.);
#7014=ADVANCED_FACE('',(#623),#240,.F.);
#7015=ADVANCED_FACE('',(#624),#241,.F.);
#7353=CLOSED_SHELL('',(#6999,#7000,#7001,#7002,#7003,#7004,#7005,#7006,
#7007));
#7354=CLOSED_SHELL('',(#7008,#7009,#7010,#7011,#7012,#7013,#7014,#7015));
#7576=AXIS2_PLACEMENT_3D('',#10305,#8322,#8323);
#7577=AXIS2_PLACEMENT_3D('',#10306,#8324,#8325);
#7578=AXIS2_PLACEMENT_3D('',#10308,#8326,#8327);
#7579=AXIS2_PLACEMENT_3D('',#10309,#8328,#8329);
#7580=AXIS2_PLACEMENT_3D('',#10311,#8330,#8331);
#7581=AXIS2_PLACEMENT_3D('',#10313,#8333,#8334);
#7582=AXIS2_PLACEMENT_3D('',#10315,#8335,#8336);
#7583=AXIS2_PLACEMENT_3D('',#10317,#8338,#8339);
#7584=AXIS2_PLACEMENT_3D('',#10319,#8340,#8341);
#7585=AXIS2_PLACEMENT_3D('',#10321,#8343,#8344);
#7586=AXIS2_PLACEMENT_3D('',#10323,#8345,#8346);
#7587=AXIS2_PLACEMENT_3D('',#10324,#8347,#8348);
#7588=AXIS2_PLACEMENT_3D('',#10326,#8349,#8350);
#7589=AXIS2_PLACEMENT_3D('',#10328,#8352,#8353);
#7590=AXIS2_PLACEMENT_3D('',#10330,#8354,#8355);
#7591=AXIS2_PLACEMENT_3D('',#10332,#8357,#8358);
#7592=AXIS2_PLACEMENT_3D('',#10334,#8359,#8360);
#7593=AXIS2_PLACEMENT_3D('',#10336,#8362,#8363);
#7594=AXIS2_PLACEMENT_3D('',#10337,#8364,#8365);
#7595=AXIS2_PLACEMENT_3D('',#10346,#8370,#8371);
#7596=AXIS2_PLACEMENT_3D('',#10352,#8375,#8376);
#7597=AXIS2_PLACEMENT_3D('',#10358,#8380,#8381);
#7598=AXIS2_PLACEMENT_3D('',#10364,#8385,#8386);
#7599=AXIS2_PLACEMENT_3D('',#10370,#8390,#8391);
#7600=AXIS2_PLACEMENT_3D('',#10373,#8394,#8395);
#7601=AXIS2_PLACEMENT_3D('',#10374,#8396,#8397);
#8322=DIRECTION('axis',(0.,0.,1.));
#8323=DIRECTION('refdir',(1.,0.,0.));
#8324=DIRECTION('center_axis',(0.,1.,0.));
#8325=DIRECTION('ref_axis',(0.,0.,1.));
#8326=DIRECTION('center_axis',(0.,-1.,0.));
#8327=DIRECTION('ref_axis',(1.,0.,0.));
#8328=DIRECTION('center_axis',(0.,-1.,0.));
#8329=DIRECTION('ref_axis',(1.,0.,0.));
#8330=DIRECTION('center_axis',(0.,-1.,0.));
#8331=DIRECTION('ref_axis',(1.,0.,0.));
#8332=DIRECTION('',(0.707106781186547,0.707106781186548,8.65956056235493E-17));
#8333=DIRECTION('center_axis',(0.,-1.,0.));
#8334=DIRECTION('ref_axis',(1.,0.,0.));
#8335=DIRECTION('center_axis',(0.,-1.,0.));
#8336=DIRECTION('ref_axis',(1.,0.,0.));
#8337=DIRECTION('',(0.,1.,0.));
#8338=DIRECTION('center_axis',(0.,1.,0.));
#8339=DIRECTION('ref_axis',(1.,0.,0.));
#8340=DIRECTION('center_axis',(0.,-1.,0.));
#8341=DIRECTION('ref_axis',(1.,0.,0.));
#8342=DIRECTION('',(-0.707106781186547,0.707106781186548,-8.65956056235493E-17));
#8343=DIRECTION('center_axis',(0.,-1.,0.));
#8344=DIRECTION('ref_axis',(0.,0.,-1.));
#8345=DIRECTION('center_axis',(0.,-1.,0.));
#8346=DIRECTION('ref_axis',(1.,0.,0.));
#8347=DIRECTION('center_axis',(0.,1.,0.));
#8348=DIRECTION('ref_axis',(1.,0.,0.));
#8349=DIRECTION('center_axis',(0.,1.,0.));
#8350=DIRECTION('ref_axis',(1.,0.,0.));
#8351=DIRECTION('',(-0.447213595499958,0.894427190999916,-5.47678698264203E-17));
#8352=DIRECTION('center_axis',(0.,-1.,0.));
#8353=DIRECTION('ref_axis',(1.,0.,0.));
#8354=DIRECTION('center_axis',(0.,1.,0.));
#8355=DIRECTION('ref_axis',(1.,0.,0.));
#8356=DIRECTION('',(0.,1.,0.));
#8357=DIRECTION('center_axis',(0.,1.,0.));
#8358=DIRECTION('ref_axis',(1.,0.,0.));
#8359=DIRECTION('center_axis',(0.,-1.,0.));
#8360=DIRECTION('ref_axis',(1.,0.,0.));
#8361=DIRECTION('',(-0.707106781186547,0.707106781186548,-8.65956056235493E-17));
#8362=DIRECTION('center_axis',(0.,-1.,0.));
#8363=DIRECTION('ref_axis',(0.,0.,-1.));
#8364=DIRECTION('center_axis',(0.866025403784439,0.,-0.5));
#8365=DIRECTION('ref_axis',(0.5,0.,0.866025403784439));
#8366=DIRECTION('',(-0.5,0.,-0.866025403784439));
#8367=DIRECTION('',(0.,-1.,0.));
#8368=DIRECTION('',(0.5,0.,0.866025403784439));
#8369=DIRECTION('',(0.,-1.,0.));
#8370=DIRECTION('center_axis',(1.60246890531964E-16,0.,-1.));
#8371=DIRECTION('ref_axis',(1.,0.,1.60246890531964E-16));
#8372=DIRECTION('',(-1.,0.,-1.60246890531964E-16));
#8373=DIRECTION('',(0.,-1.,0.));
#8374=DIRECTION('',(1.,0.,1.60246890531964E-16));
#8375=DIRECTION('center_axis',(-0.866025403784439,0.,-0.5));
#8376=DIRECTION('ref_axis',(0.5,0.,-0.866025403784439));
#8377=DIRECTION('',(-0.5,0.,0.866025403784439));
#8378=DIRECTION('',(0.,-1.,0.));
#8379=DIRECTION('',(0.5,0.,-0.866025403784439));
#8380=DIRECTION('center_axis',(-0.866025403784439,0.,0.5));
#8381=DIRECTION('ref_axis',(-0.5,0.,-0.866025403784439));
#8382=DIRECTION('',(0.5,0.,0.866025403784439));
#8383=DIRECTION('',(0.,-1.,0.));
#8384=DIRECTION('',(-0.5,0.,-0.866025403784439));
#8385=DIRECTION('center_axis',(-1.60246890531964E-16,0.,1.));
#8386=DIRECTION('ref_axis',(-1.,0.,-1.60246890531964E-16));
#8387=DIRECTION('',(1.,0.,1.60246890531964E-16));
#8388=DIRECTION('',(0.,-1.,0.));
#8389=DIRECTION('',(-1.,0.,-1.60246890531964E-16));
#8390=DIRECTION('center_axis',(0.866025403784439,0.,0.5));
#8391=DIRECTION('ref_axis',(-0.5,0.,0.866025403784439));
#8392=DIRECTION('',(0.5,0.,-0.866025403784439));
#8393=DIRECTION('',(-0.5,0.,0.866025403784439));
#8394=DIRECTION('center_axis',(0.,1.,0.));
#8395=DIRECTION('ref_axis',(1.,0.,0.));
#8396=DIRECTION('center_axis',(0.,-1.,0.));
#8397=DIRECTION('ref_axis',(0.,0.,-1.));
#10305=CARTESIAN_POINT('',(0.,0.,0.));
#10306=CARTESIAN_POINT('Origin',(0.3,0.4,0.));
#10307=CARTESIAN_POINT('',(-0.3,0.4,-3.67394039744206E-17));
#10308=CARTESIAN_POINT('Origin',(0.,0.4,0.));
#10309=CARTESIAN_POINT('Origin',(0.,0.375,0.));
#10310=CARTESIAN_POINT('',(-0.35,0.35,-4.28626379701573E-17));
#10311=CARTESIAN_POINT('Origin',(0.,0.35,0.));
#10312=CARTESIAN_POINT('',(-0.325,0.375,-3.9801020972289E-17));
#10313=CARTESIAN_POINT('Origin',(0.,0.19,0.));
#10314=CARTESIAN_POINT('',(-0.35,0.03,-4.28626379701574E-17));
#10315=CARTESIAN_POINT('Origin',(0.,0.03,0.));
#10316=CARTESIAN_POINT('',(-0.35,0.19,-4.28626379701574E-17));
#10317=CARTESIAN_POINT('Origin',(0.,0.0149999999999999,0.));
#10318=CARTESIAN_POINT('',(-0.32,-3.29597460435593E-17,-3.91886975727153E-17));
#10319=CARTESIAN_POINT('Origin',(0.,0.,0.));
#10320=CARTESIAN_POINT('',(-0.335,0.0149999999999999,-4.10256677714363E-17));
#10321=CARTESIAN_POINT('Origin',(0.22,0.,0.));
#10322=CARTESIAN_POINT('',(-0.22,-6.93889390390723E-18,-2.69422295812418E-17));
#10323=CARTESIAN_POINT('Origin',(0.,0.,0.));
#10324=CARTESIAN_POINT('Origin',(0.,-0.02,0.));
#10325=CARTESIAN_POINT('',(-0.1954,-0.0492,2.39295984553393E-17));
#10326=CARTESIAN_POINT('Origin',(0.,-0.0492,0.));
#10327=CARTESIAN_POINT('',(-0.21,-0.02,-2.57175827820944E-17));
#10328=CARTESIAN_POINT('Origin',(0.,-0.8,0.));
#10329=CARTESIAN_POINT('',(-0.1954,-1.5646,2.39295984553393E-17));
#10330=CARTESIAN_POINT('Origin',(0.,-1.5646,0.));
#10331=CARTESIAN_POINT('',(-0.1954,-0.8,-2.39295984553393E-17));
#10332=CARTESIAN_POINT('Origin',(0.,-1.58,0.));
#10333=CARTESIAN_POINT('',(-0.16,-1.6,-1.95943487863577E-17));
#10334=CARTESIAN_POINT('Origin',(0.,-1.6,0.));
#10335=CARTESIAN_POINT('',(-0.18,-1.58,-2.20436423846524E-17));
#10336=CARTESIAN_POINT('Origin',(0.,-1.6,0.));
#10337=CARTESIAN_POINT('Origin',(0.0866025403784439,-0.4,-0.15));
#10338=CARTESIAN_POINT('',(0.173205080756888,-0.4,0.));
#10339=CARTESIAN_POINT('',(0.0866025403784439,-0.4,-0.15));
#10340=CARTESIAN_POINT('',(0.173205080756888,-0.4,0.));
#10341=CARTESIAN_POINT('',(0.0866025403784439,-0.64,-0.15));
#10342=CARTESIAN_POINT('',(0.0866025403784439,-0.4,-0.15));
#10343=CARTESIAN_POINT('',(0.173205080756888,-0.64,0.));
#10344=CARTESIAN_POINT('',(0.173205080756888,-0.64,0.));
#10345=CARTESIAN_POINT('',(0.173205080756888,-0.4,0.));
#10346=CARTESIAN_POINT('Origin',(-0.0866025403784438,-0.4,-0.15));
#10347=CARTESIAN_POINT('',(-0.0866025403784438,-0.4,-0.15));
#10348=CARTESIAN_POINT('',(0.0866025403784439,-0.4,-0.15));
#10349=CARTESIAN_POINT('',(-0.0866025403784438,-0.64,-0.15));
#10350=CARTESIAN_POINT('',(-0.0866025403784438,-0.4,-0.15));
#10351=CARTESIAN_POINT('',(0.0866025403784439,-0.64,-0.15));
#10352=CARTESIAN_POINT('Origin',(-0.173205080756888,-0.4,-2.77555756156289E-17));
#10353=CARTESIAN_POINT('',(-0.173205080756888,-0.4,-2.12115047744981E-17));
#10354=CARTESIAN_POINT('',(-0.0866025403784438,-0.4,-0.15));
#10355=CARTESIAN_POINT('',(-0.173205080756888,-0.64,-2.77555756156289E-17));
#10356=CARTESIAN_POINT('',(-0.173205080756888,-0.4,-2.12115047744981E-17));
#10357=CARTESIAN_POINT('',(-0.0866025403784438,-0.64,-0.15));
#10358=CARTESIAN_POINT('Origin',(-0.0866025403784439,-0.4,0.15));
#10359=CARTESIAN_POINT('',(-0.0866025403784439,-0.4,0.15));
#10360=CARTESIAN_POINT('',(-0.173205080756888,-0.4,-2.12115047744981E-17));
#10361=CARTESIAN_POINT('',(-0.0866025403784439,-0.64,0.15));
#10362=CARTESIAN_POINT('',(-0.0866025403784439,-0.4,0.15));
#10363=CARTESIAN_POINT('',(-0.173205080756888,-0.64,-2.12115047744981E-17));
#10364=CARTESIAN_POINT('Origin',(0.0866025403784439,-0.4,0.15));
#10365=CARTESIAN_POINT('',(0.0866025403784439,-0.4,0.15));
#10366=CARTESIAN_POINT('',(-0.0866025403784439,-0.4,0.15));
#10367=CARTESIAN_POINT('',(0.0866025403784439,-0.64,0.15));
#10368=CARTESIAN_POINT('',(0.0866025403784439,-0.4,0.15));
#10369=CARTESIAN_POINT('',(-0.0866025403784439,-0.64,0.15));
#10370=CARTESIAN_POINT('Origin',(0.173205080756888,-0.4,0.));
#10371=CARTESIAN_POINT('',(0.0866025403784439,-0.4,0.15));
#10372=CARTESIAN_POINT('',(0.0866025403784439,-0.64,0.15));
#10373=CARTESIAN_POINT('Origin',(0.,-0.4,-2.77555756156289E-17));
#10374=CARTESIAN_POINT('Origin',(0.,-0.64,-2.77555756156289E-17));
#12322=UNCERTAINTY_MEASURE_WITH_UNIT(LENGTH_MEASURE(0.001),#12344,
'DISTANCE_ACCURACY_VALUE',
'Maximum model space distance between geometric entities at asserted c
onnectivities');
#12329=UNCERTAINTY_MEASURE_WITH_UNIT(LENGTH_MEASURE(0.001),#12344,
'DISTANCE_ACCURACY_VALUE',
'Maximum model space distance between geometric entities at asserted c
onnectivities');
#12336=(
GEOMETRIC_REPRESENTATION_CONTEXT(3)
GLOBAL_UNCERTAINTY_ASSIGNED_CONTEXT((#12322))
GLOBAL_UNIT_ASSIGNED_CONTEXT((#12344,#12346,#12347))
REPRESENTATION_CONTEXT('','3D')
);
#12343=(
GEOMETRIC_REPRESENTATION_CONTEXT(3)
GLOBAL_UNCERTAINTY_ASSIGNED_CONTEXT((#12329))
GLOBAL_UNIT_ASSIGNED_CONTEXT((#12344,#12346,#12347))
REPRESENTATION_CONTEXT('','3D')
);
#12344=(
LENGTH_UNIT()
NAMED_UNIT(*)
SI_UNIT(.CENTI.,.METRE.)
);
#12346=(
NAMED_UNIT(*)
PLANE_ANGLE_UNIT()
SI_UNIT($,.RADIAN.)
);
#12347=(
NAMED_UNIT(*)
SI_UNIT($,.STERADIAN.)
SOLID_ANGLE_UNIT()
);
#12354=SHAPE_DEFINITION_REPRESENTATION(#12367,#12401);
#12367=PRODUCT_DEFINITION_SHAPE('',$,#12415);
#12401=SHAPE_REPRESENTATION('',(#7576),#12336);
#12408=PRODUCT_DEFINITION_CONTEXT('part definition',#12449,'design');
#12415=PRODUCT_DEFINITION('Cap Screw - M4x16',
'Cap Screw - M4x16',#12428,#12408);
#12428=PRODUCT_DEFINITION_FORMATION('',$,#12457);
#12449=APPLICATION_CONTEXT(
'Core Data for Automotive Mechanical Design Process');
#12450=PRODUCT_CONTEXT('part definition',#12449,'mechanical');
#12457=PRODUCT('Cap Screw - M4x16','Cap Screw - M4x16',
'Cap Screw - M4x16',(#12450));
#12534=COLOUR_RGB('Black',0.12,0.14,0.17);
#12535=FILL_AREA_STYLE_COLOUR('',#12534);
#12536=FILL_AREA_STYLE('',(#12535));
#12537=SURFACE_STYLE_FILL_AREA(#12536);
#12538=SURFACE_SIDE_STYLE('',(#12537));
#12539=SURFACE_STYLE_USAGE(.BOTH.,#12538);
#12540=PRESENTATION_STYLE_ASSIGNMENT((#12539));
ENDSEC;
END-ISO-10303-21;
